ISO-10303-21;
HEADER;
FILE_DESCRIPTION (('STEP AP214'),
    '1' );
FILE_NAME ('socket head cap screw_iso_ISO 4762 M10 x 40 - 40N.step',
    '2026-10-31T03:46:07',
    ( '' ),
    ( '' ),
    'SwSTEP 2.0',
    'SolidWorks 2026',
    '' );
FILE_SCHEMA (( 'AUTOMOTIVE_DESIGN' ));
ENDSEC;

DATA;
#5=EDGE_LOOP ( 'NONE', ( #366, #3432, #8701, #5871, #3805 ) ) ;
#26=EDGE_CURVE ( 'NONE', #18313, #7126, #7119, .T. ) ;
#93=ORIENTED_EDGE ( 'NONE', *, *, #8723, .F. ) ;
#105=ORIENTED_EDGE ( 'NONE', *, *, #5663, .T. ) ;
#183=EDGE_CURVE ( 'NONE', #1893, #16800, #2084, .T. ) ;
#191=VECTOR ( 'NONE', #8346, 999.9999999999998863 ) ;
#197=LINE ( 'NONE', #22401, #4609 ) ;
#232=EDGE_LOOP ( 'NONE', ( #16649, #15723, #18721 ) ) ;
#239=EDGE_LOOP ( 'NONE', ( #13471, #13431, #11953, #18524 ) ) ;
#252=ORIENTED_EDGE ( 'NONE', *, *, #20392, .F. ) ;
#260=CARTESIAN_POINT ( 'NONE',  ( 49.17200000000001836, 0.000000000000000000, 5.000000000000002665 ) ) ;
#305=EDGE_CURVE ( 'NONE', #16453, #7964, #16042, .T. ) ;
#315=DIRECTION ( 'NONE',  ( 0.000000000000000000, 0.000000000000000000, 1.000000000000000000 ) ) ;
#330=CARTESIAN_POINT ( 'NONE',  ( 5.000000000000000000, 4.685197434473814759, -5.637851296924623057E-15 ) ) ;
#366=ORIENTED_EDGE ( 'NONE', *, *, #7485, .F. ) ;
#374=AXIS2_PLACEMENT_3D ( 'NONE', #18299, #13274, #11090 ) ;
#377=EDGE_LOOP ( 'NONE', ( #20981, #9413, #16535, #22463, #1833 ) ) ;
#397=VECTOR ( 'NONE', #5693, 1000.000000000000000 ) ;
#437=LINE ( 'NONE', #21907, #19401 ) ;
#454=ORIENTED_EDGE ( 'NONE', *, *, #4695, .F. ) ;
#470=CARTESIAN_POINT ( 'NONE',  ( 0.000000000000000000, 4.685197434473814759, -5.637851296924623057E-15 ) ) ;
#491=DIRECTION ( 'NONE',  ( 0.000000000000000000, 0.000000000000000000, -1.000000000000000000 ) ) ;
#580=EDGE_CURVE ( 'NONE', #1699, #1893, #14858, .T. ) ;
#583=DIRECTION ( 'NONE',  ( -0.000000000000000000, 0.000000000000000000, 1.000000000000000000 ) ) ;
#613=EDGE_CURVE ( 'NONE', #10116, #16453, #2122, .T. ) ;
#628=DIRECTION ( 'NONE',  ( 1.000000000000000000, 0.000000000000000000, 0.000000000000000000 ) ) ;
#653=ORIENTED_EDGE ( 'NONE', *, *, #14771, .F. ) ;
#747=EDGE_CURVE ( 'NONE', #1893, #4175, #10354, .T. ) ;
#748=VERTEX_POINT ( 'NONE', #19617 ) ;
#818=FACE_BOUND ( 'NONE', #20184, .T. ) ;
#839=EDGE_LOOP ( 'NONE', ( #4051, #13336, #850, #10609, #14408 ) ) ;
#850=ORIENTED_EDGE ( 'NONE', *, *, #20757, .T. ) ;
#852=VERTEX_POINT ( 'NONE', #10959 ) ;
#966=ORIENTED_EDGE ( 'NONE', *, *, #21059, .F. ) ;
#980=CARTESIAN_POINT ( 'NONE',  ( 50.00000000000000000, 0.000000000000000000, 0.000000000000000000 ) ) ;
#1005=ORIENTED_EDGE ( 'NONE', *, *, #16733, .T. ) ;
#1018=AXIS2_PLACEMENT_3D ( 'NONE', #15491, #15361, #9695 ) ;
#1025=EDGE_CURVE ( 'NONE', #6490, #3871, #4720, .T. ) ;
#1031=VERTEX_POINT ( 'NONE', #12386 ) ;
#1045=VECTOR ( 'NONE', #15936, 999.9999999999998863 ) ;
#1059=DIRECTION ( 'NONE',  ( 0.000000000000000000, 0.000000000000000000, 1.000000000000000000 ) ) ;
#1080=VECTOR ( 'NONE', #12261, 1000.000000000000000 ) ;
#1103=VECTOR ( 'NONE', #4319, 1000.000000000000000 ) ;
#1104=DIRECTION ( 'NONE',  ( 0.000000000000000000, 0.000000000000000000, -1.000000000000000000 ) ) ;
#1309=DIRECTION ( 'NONE',  ( 1.000000000000000000, 0.000000000000000000, 0.000000000000000000 ) ) ;
#1338=ADVANCED_FACE ( 'NONE', ( #11373 ), #22809, .T. ) ;
#1451=FACE_OUTER_BOUND ( 'NONE', #6237, .T. ) ;
#1522=AXIS2_PLACEMENT_3D ( 'NONE', #19276, #14003, #13890 ) ;
#1581=CARTESIAN_POINT ( 'NONE',  ( 10.40000000000000036, 0.000000000000000000, 0.000000000000000000 ) ) ;
#1646=VECTOR ( 'NONE', #9901, 999.9999999999998863 ) ;
#1655=DIRECTION ( 'NONE',  ( 0.000000000000000000, 0.000000000000000000, 1.000000000000000000 ) ) ;
#1699=VERTEX_POINT ( 'NONE', #9396 ) ;
#1717=CARTESIAN_POINT ( 'NONE',  ( 5.000000000000000000, 0.000000000000000000, 0.000000000000000000 ) ) ;
#1773=DIRECTION ( 'NONE',  ( 0.000000000000000000, -0.5000000000000009992, -0.8660254037844380415 ) ) ;
#1775=EDGE_CURVE ( 'NONE', #7126, #6529, #9987, .T. ) ;
#1779=CARTESIAN_POINT ( 'NONE',  ( 1.500000000000001332, 0.000000000000000000, 0.000000000000000000 ) ) ;
#1793=ORIENTED_EDGE ( 'NONE', *, *, #20489, .F. ) ;
#1822=DIRECTION ( 'NONE',  ( -1.000000000000000000, -0.000000000000000000, -0.000000000000000000 ) ) ;
#1833=ORIENTED_EDGE ( 'NONE', *, *, #9070, .T. ) ;
#1842=CIRCLE ( 'NONE', #15376, 5.000000000000001776 ) ;
#1856=ORIENTED_EDGE ( 'NONE', *, *, #20103, .F. ) ;
#1893=VERTEX_POINT ( 'NONE', #6831 ) ;
#1900=DIRECTION ( 'NONE',  ( -1.000000000000000000, -0.000000000000000000, -0.000000000000000000 ) ) ;
#2084=CIRCLE ( 'NONE', #19047, 4.057500000000000107 ) ;
#2111=CARTESIAN_POINT ( 'NONE',  ( 1.500000000000001332, 7.960204194457796463E-16, -6.500000000000000888 ) ) ;
#2122=LINE ( 'NONE', #330, #4808 ) ;
#2132=ORIENTED_EDGE ( 'NONE', *, *, #5885, .F. ) ;
#2153=DIRECTION ( 'NONE',  ( 0.000000000000000000, 1.000000000000000000, -1.295896757998781966E-15 ) ) ;
#2246=DIRECTION ( 'NONE',  ( 0.000000000000000000, -1.000000000000000000, 0.000000000000000000 ) ) ;
#2347=CARTESIAN_POINT ( 'NONE',  ( 5.000000000000000000, -3.513898075855361292, -2.028749999999995168 ) ) ;
#2375=PLANE ( 'NONE',  #17845 ) ;
#2404=DIRECTION ( 'NONE',  ( 1.000000000000000000, 0.000000000000000000, 0.000000000000000000 ) ) ;
#2429=EDGE_LOOP ( 'NONE', ( #10390, #454, #8131, #8319 ) ) ;
#2481=( NAMED_UNIT ( * ) PLANE_ANGLE_UNIT ( ) SI_UNIT ( $, .RADIAN. ) );
#2492=VECTOR ( 'NONE', #13882, 1000.000000000000000 ) ;
#2559=LINE ( 'NONE', #4620, #1080 ) ;
#2562=DIRECTION ( 'NONE',  ( -1.000000000000000000, -0.000000000000000000, -0.000000000000000000 ) ) ;
#2599=VECTOR ( 'NONE', #1773, 1000.000000000000114 ) ;
#2638=ORIENTED_EDGE ( 'NONE', *, *, #16272, .T. ) ;
#2709=PRODUCT_DEFINITION_FORMATION_WITH_SPECIFIED_SOURCE ( 'ANY', '', #2824, .NOT_KNOWN. ) ;
#2742=CARTESIAN_POINT ( 'NONE',  ( 5.000000000000000000, 4.685197434473814759, -5.637851296924623057E-15 ) ) ;
#2793=DIRECTION ( 'NONE',  ( 1.000000000000000000, 0.000000000000000000, 0.000000000000000000 ) ) ;
#2824=PRODUCT ( 'socket head cap screw_iso_ISO 4762 M10 x 40 - 40N', 'socket head cap screw_iso_ISO 4762 M10 x 40 - 40N', '', ( #9407 ) ) ;
#2973=EDGE_CURVE ( 'NONE', #6750, #6295, #18922, .T. ) ;
#3034=ADVANCED_FACE ( 'NONE', ( #17712 ), #16030, .F. ) ;
#3037=CIRCLE ( 'NONE', #10027, 4.171999999999999709 ) ;
#3059=CARTESIAN_POINT ( 'NONE',  ( 5.000000000000000000, 4.685197434473814759, -5.637851296924623057E-15 ) ) ;
#3065=CONICAL_SURFACE ( 'NONE', #4991, 4.057500000000000107, 1.047197551196593857 ) ;
#3073=CARTESIAN_POINT ( 'NONE',  ( 0.000000000000000000, 8.878689293818310074E-16, -6.500000000000000888 ) ) ;
#3092=ORIENTED_EDGE ( 'NONE', *, *, #9070, .F. ) ;
#3106=DIRECTION ( 'NONE',  ( 1.000000000000000000, 0.000000000000000000, 0.000000000000000000 ) ) ;
#3139=VERTEX_POINT ( 'NONE', #19507 ) ;
#3154=LINE ( 'NONE', #18141, #3403 ) ;
#3157=VECTOR ( 'NONE', #13548, 1000.000000000000114 ) ;
#3210=DIRECTION ( 'NONE',  ( 0.000000000000000000, 0.000000000000000000, -1.000000000000000000 ) ) ;
#3217=VECTOR ( 'NONE', #15097, 1000.000000000000000 ) ;
#3236=MECHANICAL_DESIGN_GEOMETRIC_PRESENTATION_REPRESENTATION('',(#6329),#19822);
#3303=EDGE_LOOP ( 'NONE', ( #20738, #7908, #1856 ) ) ;
#3337=AXIS2_PLACEMENT_3D ( 'NONE', #15013, #628, #12988 ) ;
#3403=VECTOR ( 'NONE', #8849, 1000.000000000000000 ) ;
#3432=ORIENTED_EDGE ( 'NONE', *, *, #12453, .T. ) ;
#3487=CARTESIAN_POINT ( 'NONE',  ( -31.74999999999995737, 0.000000000000000000, 0.000000000000000000 ) ) ;
#3490=DIRECTION ( 'NONE',  ( -1.000000000000000000, -0.000000000000000000, -0.000000000000000000 ) ) ;
#3527=EDGE_LOOP ( 'NONE', ( #3784, #22324, #12867 ) ) ;
#3544=EDGE_LOOP ( 'NONE', ( #13861, #9400, #11674, #16688, #16061 ) ) ;
#3569=ORIENTED_EDGE ( 'NONE', *, *, #16613, .T. ) ;
#3582=AXIS2_PLACEMENT_3D ( 'NONE', #13644, #4890, #19370 ) ;
#3653=ORIENTED_EDGE ( 'NONE', *, *, #4860, .T. ) ;
#3769=DIRECTION ( 'NONE',  ( 1.000000000000000000, 0.000000000000000000, 0.000000000000000000 ) ) ;
#3784=ORIENTED_EDGE ( 'NONE', *, *, #7127, .F. ) ;
#3805=ORIENTED_EDGE ( 'NONE', *, *, #305, .T. ) ;
#3863=FACE_OUTER_BOUND ( 'NONE', #21133, .T. ) ;
#3871=VERTEX_POINT ( 'NONE', #23586 ) ;
#3895=LINE ( 'NONE', #18264, #12893 ) ;
#3918=CARTESIAN_POINT ( 'NONE',  ( 10.00000000000000000, 6.613092715395708453E-16, 5.400000000000002132 ) ) ;
#3939=DIRECTION ( 'NONE',  ( 0.000000000000000000, -0.8660254037844391517, -0.4999999999999991673 ) ) ;
#3943=EDGE_CURVE ( 'NONE', #16453, #3139, #14780, .T. ) ;
#3964=PLANE ( 'NONE',  #17502 ) ;
#3987=CARTESIAN_POINT ( 'NONE',  ( 5.000000000000000000, 3.513898075855363068, 2.028749999999996945 ) ) ;
#4004=FACE_OUTER_BOUND ( 'NONE', #22363, .T. ) ;
#4051=ORIENTED_EDGE ( 'NONE', *, *, #1025, .F. ) ;
#4054=CARTESIAN_POINT ( 'NONE',  ( 1.500000000000001332, 0.000000000000000000, 8.000000000000000000 ) ) ;
#4063=CARTESIAN_POINT ( 'NONE',  ( 0.000000000000000000, 0.000000000000000000, 0.000000000000000000 ) ) ;
#4118=AXIS2_PLACEMENT_3D ( 'NONE', #19766, #12217, #10143 ) ;
#4139=CARTESIAN_POINT ( 'NONE',  ( 5.000000000000000000, 3.513898075855358627, -2.028750000000004938 ) ) ;
#4158=VERTEX_POINT ( 'NONE', #23069 ) ;
#4175=VERTEX_POINT ( 'NONE', #6779 ) ;
#4194=FACE_OUTER_BOUND ( 'NONE', #13985, .T. ) ;
#4247=FACE_OUTER_BOUND ( 'NONE', #4678, .T. ) ;
#4296=ADVANCED_FACE ( 'NONE', ( #1451 ), #20236, .F. ) ;
#4300=FACE_OUTER_BOUND ( 'NONE', #5, .T. ) ;
#4319=DIRECTION ( 'NONE',  ( -1.000000000000000000, -0.000000000000000000, -0.000000000000000000 ) ) ;
#4339=VERTEX_POINT ( 'NONE', #11143 ) ;
#4341=CONICAL_SURFACE ( 'NONE', #22446, 4.171999999999999709, 0.7853981633974613796 ) ;
#4379=DIRECTION ( 'NONE',  ( 0.000000000000000000, 0.000000000000000000, 1.000000000000000000 ) ) ;
#4464=ADVANCED_FACE ( 'NONE', ( #15349 ), #22685, .T. ) ;
#4501=DIRECTION ( 'NONE',  ( 0.000000000000000000, 0.000000000000000000, 1.000000000000000000 ) ) ;
#4520=DIRECTION ( 'NONE',  ( 0.000000000000000000, 0.5000000000000011102, 0.8660254037844380415 ) ) ;
#4533=( LENGTH_UNIT ( ) NAMED_UNIT ( * ) SI_UNIT ( .MILLI., .METRE. ) );
#4545=DIRECTION ( 'NONE',  ( -1.000000000000000000, -0.000000000000000000, -0.000000000000000000 ) ) ;
#4609=VECTOR ( 'NONE', #11699, 1000.000000000000000 ) ;
#4617=ORIENTED_EDGE ( 'NONE', *, *, #23070, .F. ) ;
#4620=CARTESIAN_POINT ( 'NONE',  ( 5.000000000000000000, 2.342598717236902939, -4.057500000000001883 ) ) ;
#4641=CARTESIAN_POINT ( 'NONE',  ( 5.000000000000000000, 0.000000000000000000, 0.000000000000000000 ) ) ;
#4678=EDGE_LOOP ( 'NONE', ( #15846, #11720, #3653, #7925 ) ) ;
#4688=EDGE_CURVE ( 'NONE', #748, #4158, #13158, .T. ) ;
#4695=EDGE_CURVE ( 'NONE', #7126, #6295, #10256, .T. ) ;
#4718=DIRECTION ( 'NONE',  ( 0.000000000000000000, -0.4999999999999991118, 0.8660254037844391517 ) ) ;
#4720=LINE ( 'NONE', #16207, #191 ) ;
#4738=ORIENTED_EDGE ( 'NONE', *, *, #21408, .F. ) ;
#4799=FACE_OUTER_BOUND ( 'NONE', #17556, .T. ) ;
#4808=VECTOR ( 'NONE', #9757, 1000.000000000000114 ) ;
#4835=AXIS2_PLACEMENT_3D ( 'NONE', #13084, #11378, #11270 ) ;
#4860=EDGE_CURVE ( 'NONE', #9995, #1031, #11849, .T. ) ;
#4866=VECTOR ( 'NONE', #10096, 999.9999999999998863 ) ;
#4890=DIRECTION ( 'NONE',  ( -0.000000000000000000, 1.295896757998781966E-15, 1.000000000000000000 ) ) ;
#4897=ORIENTED_EDGE ( 'NONE', *, *, #15337, .F. ) ;
#4900=DIRECTION ( 'NONE',  ( -1.000000000000000000, -0.000000000000000000, -0.000000000000000000 ) ) ;
#4935=DIRECTION ( 'NONE',  ( -1.000000000000000000, -0.000000000000000000, -0.000000000000000000 ) ) ;
#4991=AXIS2_PLACEMENT_3D ( 'NONE', #4641, #6681, #21296 ) ;
#5063=FACE_OUTER_BOUND ( 'NONE', #3303, .T. ) ;
#5093=ORIENTED_EDGE ( 'NONE', *, *, #4688, .F. ) ;
#5111=VERTEX_POINT ( 'NONE', #13000 ) ;
#5314=CARTESIAN_POINT ( 'NONE',  ( 50.00000000000000000, 5.616230220889763424E-16, -4.171999999999999709 ) ) ;
#5360=AXIS2_PLACEMENT_3D ( 'NONE', #1717, #23700, #21776 ) ;
#5429=CIRCLE ( 'NONE', #13565, 4.057500000000000107 ) ;
#5440=DIRECTION ( 'NONE',  ( -1.000000000000000000, -0.000000000000000000, -0.000000000000000000 ) ) ;
#5544=UNCERTAINTY_MEASURE_WITH_UNIT (LENGTH_MEASURE( 1.000000000000000082E-05 ), #10344, 'distance_accuracy_value', 'NONE');
#5555=DIRECTION ( 'NONE',  ( 0.000000000000000000, 0.000000000000000000, -1.000000000000000000 ) ) ;
#5639=CARTESIAN_POINT ( 'NONE',  ( 5.000000000000000000, 4.685197434473814759, -5.637851296924623057E-15 ) ) ;
#5663=EDGE_CURVE ( 'NONE', #5111, #10051, #8112, .T. ) ;
#5693=DIRECTION ( 'NONE',  ( -1.000000000000000000, -0.000000000000000000, -0.000000000000000000 ) ) ;
#5698=VECTOR ( 'NONE', #22282, 1000.000000000000000 ) ;
#5706=ORIENTED_EDGE ( 'NONE', *, *, #613, .T. ) ;
#5778=ORIENTED_EDGE ( 'NONE', *, *, #7182, .T. ) ;
#5780=PRODUCT_DEFINITION ( 'UNKNOWN', '', #2709, #11485 ) ;
#5784=DIRECTION ( 'NONE',  ( -1.000000000000000000, -0.000000000000000000, -0.000000000000000000 ) ) ;
#5871=ORIENTED_EDGE ( 'NONE', *, *, #5885, .T. ) ;
#5885=EDGE_CURVE ( 'NONE', #16800, #16453, #5429, .T. ) ;
#5985=DIRECTION ( 'NONE',  ( 0.000000000000000000, 0.000000000000000000, 1.000000000000000000 ) ) ;
#6009=DIRECTION ( 'NONE',  ( 0.000000000000000000, 0.000000000000000000, 1.000000000000000000 ) ) ;
#6013=CARTESIAN_POINT ( 'NONE',  ( 5.000000000000000000, 4.969004387540385421E-16, -4.057500000000000107 ) ) ;
#6117=CYLINDRICAL_SURFACE ( 'NONE', #20378, 5.000000000000001776 ) ;
#6141=CIRCLE ( 'NONE', #5360, 4.057500000000000107 ) ;
#6179=CARTESIAN_POINT ( 'NONE',  ( 5.000000000000000000, 4.685197434473814759, -5.637851296924623057E-15 ) ) ;
#6185=CARTESIAN_POINT ( 'NONE',  ( 10.40000000000000036, 0.000000000000000000, 5.000000000000001776 ) ) ;
#6237=EDGE_LOOP ( 'NONE', ( #252, #9652, #93, #18602 ) ) ;
#6262=DIRECTION ( 'NONE',  ( -1.000000000000000000, -0.000000000000000000, -0.000000000000000000 ) ) ;
#6295=VERTEX_POINT ( 'NONE', #20223 ) ;
#6329=STYLED_ITEM('',(#23927),#12057);
#6367=CARTESIAN_POINT ( 'NONE',  ( 1.500000000000001332, 0.000000000000000000, 0.000000000000000000 ) ) ;
#6462=ORIENTED_EDGE ( 'NONE', *, *, #26, .F. ) ;
#6490=VERTEX_POINT ( 'NONE', #15302 ) ;
#6502=EDGE_CURVE ( 'NONE', #4339, #9995, #197, .T. ) ;
#6519=AXIS2_PLACEMENT_3D ( 'NONE', #14469, #19515, #3210 ) ;
#6529=VERTEX_POINT ( 'NONE', #9379 ) ;
#6562=VERTEX_POINT ( 'NONE', #3918 ) ;
#6654=ORIENTED_EDGE ( 'NONE', *, *, #5663, .F. ) ;
#6681=DIRECTION ( 'NONE',  ( -1.000000000000000000, -0.000000000000000000, -0.000000000000000000 ) ) ;
#6712=LINE ( 'NONE', #21435, #8461 ) ;
#6725=( NAMED_UNIT ( * ) SI_UNIT ( $, .STERADIAN. ) SOLID_ANGLE_UNIT ( ) );
#6742=CARTESIAN_POINT ( 'NONE',  ( 5.000000000000000000, 4.685197434473814759, -5.637851296924623057E-15 ) ) ;
#6750=VERTEX_POINT ( 'NONE', #7488 ) ;
#6779=CARTESIAN_POINT ( 'NONE',  ( 5.000000000000000000, 2.342598717236912709, 4.057499999999995666 ) ) ;
#6792=ORIENTED_EDGE ( 'NONE', *, *, #16898, .F. ) ;
#6831=CARTESIAN_POINT ( 'NONE',  ( 5.000000000000000000, 5.258101095580057891E-15, 4.057499999999999218 ) ) ;
#6918=CONICAL_SURFACE ( 'NONE', #9643, 4.057500000000000107, 1.047197551196593857 ) ;
#6986=LINE ( 'NONE', #20233, #21963 ) ;
#7042=CARTESIAN_POINT ( 'NONE',  ( 5.000000000000000000, 4.685197434473814759, -5.637851296924623057E-15 ) ) ;
#7095=ADVANCED_FACE ( 'NONE', ( #9882 ), #4341, .T. ) ;
#7098=ADVANCED_FACE ( 'NONE', ( #13408 ), #2375, .F. ) ;
#7119=LINE ( 'NONE', #10780, #9855 ) ;
#7121=VECTOR ( 'NONE', #2153, 1000.000000000000000 ) ;
#7126=VERTEX_POINT ( 'NONE', #4054 ) ;
#7127=EDGE_CURVE ( 'NONE', #748, #1699, #22653, .T. ) ;
#7180=DIRECTION ( 'NONE',  ( 0.000000000000000000, 0.000000000000000000, 1.000000000000000000 ) ) ;
#7182=EDGE_CURVE ( 'NONE', #6529, #23723, #8600, .T. ) ;
#7238=CARTESIAN_POINT ( 'NONE',  ( 5.000000000000000000, -2.342598717236900718, 4.057500000000001883 ) ) ;
#7264=CIRCLE ( 'NONE', #8064, 5.000000000000002665 ) ;
#7479=ORIENTED_EDGE ( 'NONE', *, *, #4688, .T. ) ;
#7485=EDGE_CURVE ( 'NONE', #852, #7964, #9775, .T. ) ;
#7488=CARTESIAN_POINT ( 'NONE',  ( 10.00000000000000178, 9.797174393178825657E-16, -8.000000000000000000 ) ) ;
#7499=CARTESIAN_POINT ( 'NONE',  ( 5.000000000000000000, 2.342598717236912709, 4.057499999999995666 ) ) ;
#7524=ORIENTED_EDGE ( 'NONE', *, *, #9487, .T. ) ;
#7543=CARTESIAN_POINT ( 'NONE',  ( 1.500000000000001332, 0.000000000000000000, 0.000000000000000000 ) ) ;
#7559=CARTESIAN_POINT ( 'NONE',  ( 5.000000000000000000, 2.342598717236902939, -4.057500000000001883 ) ) ;
#7631=ORIENTED_EDGE ( 'NONE', *, *, #15873, .F. ) ;
#7664=CARTESIAN_POINT ( 'NONE',  ( 5.000000000000000000, -2.342598717236900718, 4.057500000000001883 ) ) ;
#7667=AXIS2_PLACEMENT_3D ( 'NONE', #6742, #22705, #13592 ) ;
#7771=CARTESIAN_POINT ( 'NONE',  ( 0.000000000000000000, -2.342598717236900718, 4.057500000000001883 ) ) ;
#7819=EDGE_LOOP ( 'NONE', ( #21601, #18591, #7524, #4617 ) ) ;
#7840=CARTESIAN_POINT ( 'NONE',  ( 5.000000000000000000, 0.000000000000000000, 0.000000000000000000 ) ) ;
#7852=CARTESIAN_POINT ( 'NONE',  ( 0.000000000000000000, 4.685197434473814759, -5.637851296924623057E-15 ) ) ;
#7871=EDGE_CURVE ( 'NONE', #6295, #23723, #12897, .T. ) ;
#7908=ORIENTED_EDGE ( 'NONE', *, *, #21588, .F. ) ;
#7918=CARTESIAN_POINT ( 'NONE',  ( 49.17200000000001836, 0.000000000000000000, 0.000000000000000000 ) ) ;
#7921=DIRECTION ( 'NONE',  ( -0.000000000000000000, 1.000000000000000000, 1.224646799147353207E-16 ) ) ;
#7925=ORIENTED_EDGE ( 'NONE', *, *, #19898, .F. ) ;
#7938=CARTESIAN_POINT ( 'NONE',  ( 5.000000000000000000, -2.342598717236900718, 4.057500000000001883 ) ) ;
#7939=ADVANCED_FACE ( 'NONE', ( #23234 ), #10480, .F. ) ;
#7964=VERTEX_POINT ( 'NONE', #14100 ) ;
#7969=LINE ( 'NONE', #15120, #9796 ) ;
#7989=PLANE ( 'NONE',  #11135 ) ;
#7999=CIRCLE ( 'NONE', #4118, 5.400000000000002132 ) ;
#8039=CARTESIAN_POINT ( 'NONE',  ( 10.00000000000000000, 0.000000000000000000, 0.000000000000000000 ) ) ;
#8064=AXIS2_PLACEMENT_3D ( 'NONE', #7918, #16852, #315 ) ;
#8067=DIRECTION ( 'NONE',  ( 0.000000000000000000, 0.000000000000000000, -1.000000000000000000 ) ) ;
#8082=UNCERTAINTY_MEASURE_WITH_UNIT (LENGTH_MEASURE( 1.000000000000000082E-05 ), #15917, 'distance_accuracy_value', 'NONE');
#8096=CARTESIAN_POINT ( 'NONE',  ( 5.000000000000000000, 0.000000000000000000, 0.000000000000000000 ) ) ;
#8112=LINE ( 'NONE', #7852, #16209 ) ;
#8131=ORIENTED_EDGE ( 'NONE', *, *, #1775, .T. ) ;
#8176=DIRECTION ( 'NONE',  ( -1.000000000000000000, -0.000000000000000000, -0.000000000000000000 ) ) ;
#8179=( NAMED_UNIT ( * ) SI_UNIT ( $, .STERADIAN. ) SOLID_ANGLE_UNIT ( ) );
#8272=CARTESIAN_POINT ( 'NONE',  ( 10.40000000000000036, 0.000000000000000000, -5.400000000000002132 ) ) ;
#8275=EDGE_CURVE ( 'NONE', #16958, #6562, #18013, .T. ) ;
#8319=ORIENTED_EDGE ( 'NONE', *, *, #16272, .F. ) ;
#8346=DIRECTION ( 'NONE',  ( 0.000000000000000000, 0.4999999999999989453, -0.8660254037844393737 ) ) ;
#8348=EDGE_LOOP ( 'NONE', ( #20676, #22808 ) ) ;
#8395=FILL_AREA_STYLE_COLOUR ( '', #10026 ) ;
#8423=AXIS2_PLACEMENT_3D ( 'NONE', #10719, #14804, #8902 ) ;
#8461=VECTOR ( 'NONE', #4900, 1000.000000000000000 ) ;
#8464=VECTOR ( 'NONE', #16590, 1000.000000000000114 ) ;
#8495=AXIS2_PLACEMENT_3D ( 'NONE', #22492, #22246, #22612 ) ;
#8531=SURFACE_SIDE_STYLE ('',( #13647 ) ) ;
#8568=LINE ( 'NONE', #9040, #1045 ) ;
#8600=CIRCLE ( 'NONE', #23627, 6.500000000000000888 ) ;
#8701=ORIENTED_EDGE ( 'NONE', *, *, #183, .T. ) ;
#8723=EDGE_CURVE ( 'NONE', #1031, #6562, #7999, .T. ) ;
#8780=DIRECTION ( 'NONE',  ( -1.000000000000000000, -0.000000000000000000, -0.000000000000000000 ) ) ;
#8809=VECTOR ( 'NONE', #18192, 1000.000000000000000 ) ;
#8827=AXIS2_PLACEMENT_3D ( 'NONE', #10364, #10244, #21450 ) ;
#8846=DIRECTION ( 'NONE',  ( -1.000000000000000000, -0.000000000000000000, -0.000000000000000000 ) ) ;
#8849=DIRECTION ( 'NONE',  ( 0.000000000000000000, -1.000000000000000000, 9.256405414277014607E-16 ) ) ;
#8902=DIRECTION ( 'NONE',  ( 0.000000000000000000, 0.000000000000000000, 1.000000000000000000 ) ) ;
#8915=FACE_OUTER_BOUND ( 'NONE', #17534, .T. ) ;
#8947=ORIENTED_EDGE ( 'NONE', *, *, #11829, .T. ) ;
#8985=ADVANCED_FACE ( 'NONE', ( #17106 ), #22519, .F. ) ;
#9040=CARTESIAN_POINT ( 'NONE',  ( 50.00000000000000000, 5.109226446042757607E-16, -4.171999999999999709 ) ) ;
#9070=EDGE_CURVE ( 'NONE', #3139, #10051, #13278, .T. ) ;
#9101=ORIENTED_EDGE ( 'NONE', *, *, #11417, .F. ) ;
#9183=UNCERTAINTY_MEASURE_WITH_UNIT (LENGTH_MEASURE( 1.000000000000000082E-05 ), #4533, 'distance_accuracy_value', 'NONE');
#9238=CIRCLE ( 'NONE', #17338, 4.171999999999999709 ) ;
#9379=CARTESIAN_POINT ( 'NONE',  ( 0.000000000000000000, 0.000000000000000000, 6.500000000000000888 ) ) ;
#9385=AXIS2_PLACEMENT_3D ( 'NONE', #2111, #7921, #9503 ) ;
#9396=CARTESIAN_POINT ( 'NONE',  ( 5.000000000000000000, -3.513898075855356407, 2.028750000000003162 ) ) ;
#9400=ORIENTED_EDGE ( 'NONE', *, *, #7485, .T. ) ;
#9401=CARTESIAN_POINT ( 'NONE',  ( 5.000000000000000000, -2.342598717236900718, 4.057500000000001883 ) ) ;
#9406=FACE_OUTER_BOUND ( 'NONE', #22866, .T. ) ;
#9407=PRODUCT_CONTEXT ( 'NONE', #20150, 'mechanical' ) ;
#9413=ORIENTED_EDGE ( 'NONE', *, *, #10982, .F. ) ;
#9473=CARTESIAN_POINT ( 'NONE',  ( 0.000000000000000000, 0.000000000000000000, 0.000000000000000000 ) ) ;
#9487=EDGE_CURVE ( 'NONE', #9995, #16958, #12401, .T. ) ;
#9503=DIRECTION ( 'NONE',  ( 0.000000000000000000, -1.224646799147353454E-16, 1.000000000000000000 ) ) ;
#9515=DIRECTION ( 'NONE',  ( 0.000000000000000000, 0.000000000000000000, -1.000000000000000000 ) ) ;
#9570=ORIENTED_EDGE ( 'NONE', *, *, #21408, .T. ) ;
#9633=DIRECTION ( 'NONE',  ( 0.000000000000000000, -9.256405414277014607E-16, -1.000000000000000000 ) ) ;
#9641=AXIS2_PLACEMENT_3D ( 'NONE', #3059, #19596, #4520 ) ;
#9643=AXIS2_PLACEMENT_3D ( 'NONE', #22772, #8176, #5985 ) ;
#9652=ORIENTED_EDGE ( 'NONE', *, *, #8275, .T. ) ;
#9680=AXIS2_PLACEMENT_3D ( 'NONE', #15281, #22613, #13369 ) ;
#9695=DIRECTION ( 'NONE',  ( 0.000000000000000000, 1.224646799147353207E-16, 1.000000000000000000 ) ) ;
#9757=DIRECTION ( 'NONE',  ( 0.000000000000000000, -0.5000000000000011102, -0.8660254037844379305 ) ) ;
#9770=DIRECTION ( 'NONE',  ( -1.000000000000000000, 0.000000000000000000, -0.000000000000000000 ) ) ;
#9775=LINE ( 'NONE', #6013, #1646 ) ;
#9796=VECTOR ( 'NONE', #18693, 1000.000000000000000 ) ;
#9855=VECTOR ( 'NONE', #5440, 1000.000000000000000 ) ;
#9875=FACE_OUTER_BOUND ( 'NONE', #7819, .T. ) ;
#9882=FACE_OUTER_BOUND ( 'NONE', #9925, .T. ) ;
#9883=EDGE_CURVE ( 'NONE', #4175, #16275, #22220, .T. ) ;
#9901=DIRECTION ( 'NONE',  ( -0.5000000000000034417, 1.060575238724904696E-16, -0.8660254037844367092 ) ) ;
#9925=EDGE_LOOP ( 'NONE', ( #9570, #23058, #22459, #13401 ) ) ;
#9959=ADVANCED_FACE ( 'NONE', ( #5063 ), #21604, .F. ) ;
#9987=CIRCLE ( 'NONE', #13849, 1.499999999999999556 ) ;
#9995=VERTEX_POINT ( 'NONE', #20902 ) ;
#10026=COLOUR_RGB ( '',1.000000000000000000, 0.9490196078431372140, 0.9098039215686274384 ) ;
#10027=AXIS2_PLACEMENT_3D ( 'NONE', #18979, #2562, #4379 ) ;
#10051=VERTEX_POINT ( 'NONE', #10517 ) ;
#10096=DIRECTION ( 'NONE',  ( -0.7071067811865383579, 0.000000000000000000, 0.7071067811865567876 ) ) ;
#10110=ORIENTED_EDGE ( 'NONE', *, *, #2973, .T. ) ;
#10116=VERTEX_POINT ( 'NONE', #5639 ) ;
#10143=DIRECTION ( 'NONE',  ( 0.000000000000000000, 0.000000000000000000, -1.000000000000000000 ) ) ;
#10157=ORIENTED_EDGE ( 'NONE', *, *, #21474, .F. ) ;
#10244=DIRECTION ( 'NONE',  ( 1.000000000000000000, 0.000000000000000000, 0.000000000000000000 ) ) ;
#10256=CIRCLE ( 'NONE', #11420, 8.000000000000000000 ) ;
#10282=DIRECTION ( 'NONE',  ( 0.000000000000000000, 1.000000000000000000, -1.295896757998781966E-15 ) ) ;
#10283=CARTESIAN_POINT ( 'NONE',  ( 0.000000000000000000, 0.000000000000000000, 0.000000000000000000 ) ) ;
#10319=ADVANCED_FACE ( 'NONE', ( #9875 ), #6117, .T. ) ;
#10344=( LENGTH_UNIT ( ) NAMED_UNIT ( * ) SI_UNIT ( .MILLI., .METRE. ) );
#10354=LINE ( 'NONE', #17697, #2492 ) ;
#10364=CARTESIAN_POINT ( 'NONE',  ( 5.000000000000000000, 4.685197434473814759, -5.637851296924623057E-15 ) ) ;
#10378=FACE_OUTER_BOUND ( 'NONE', #19062, .T. ) ;
#10390=ORIENTED_EDGE ( 'NONE', *, *, #7871, .F. ) ;
#10445=DIRECTION ( 'NONE',  ( -1.000000000000000000, -0.000000000000000000, -0.000000000000000000 ) ) ;
#10480=PLANE ( 'NONE',  #3582 ) ;
#10508=DIRECTION ( 'NONE',  ( 0.000000000000000000, 0.000000000000000000, -1.000000000000000000 ) ) ;
#10514=EDGE_CURVE ( 'NONE', #12610, #6490, #6712, .T. ) ;
#10517=CARTESIAN_POINT ( 'NONE',  ( 0.000000000000000000, 2.342598717236902939, -4.057500000000001883 ) ) ;
#10518=FACE_OUTER_BOUND ( 'NONE', #232, .T. ) ;
#10579=LINE ( 'NONE', #7238, #7121 ) ;
#10609=ORIENTED_EDGE ( 'NONE', *, *, #21588, .T. ) ;
#10610=CARTESIAN_POINT ( 'NONE',  ( 50.00000000000000000, 0.000000000000000000, 0.000000000000000000 ) ) ;
#10713=( NAMED_UNIT ( * ) PLANE_ANGLE_UNIT ( ) SI_UNIT ( $, .RADIAN. ) );
#10719=CARTESIAN_POINT ( 'NONE',  ( 0.000000000000000000, 0.000000000000000000, 0.000000000000000000 ) ) ;
#10741=AXIS2_PLACEMENT_3D ( 'NONE', #18549, #21933, #1655 ) ;
#10780=CARTESIAN_POINT ( 'NONE',  ( -31.74999999999995737, 0.000000000000000000, 8.000000000000000000 ) ) ;
#10806=( GEOMETRIC_REPRESENTATION_CONTEXT ( 3 ) GLOBAL_UNCERTAINTY_ASSIGNED_CONTEXT ( ( #5544 ) ) GLOBAL_UNIT_ASSIGNED_CONTEXT ( ( #10344, #10713, #16257 ) ) REPRESENTATION_CONTEXT ( 'NONE', 'WORKASPACE' ) );
#10811=ADVANCED_FACE ( 'NONE', ( #13974 ), #3065, .F. ) ;
#10864=( NAMED_UNIT ( * ) PLANE_ANGLE_UNIT ( ) SI_UNIT ( $, .RADIAN. ) );
#10959=CARTESIAN_POINT ( 'NONE',  ( 7.342598717236928252, 0.000000000000000000, 0.000000000000000000 ) ) ;
#10964=DIRECTION ( 'NONE',  ( -1.000000000000000000, -0.000000000000000000, -0.000000000000000000 ) ) ;
#10982=EDGE_CURVE ( 'NONE', #22508, #3871, #437, .T. ) ;
#11090=DIRECTION ( 'NONE',  ( 0.000000000000000000, 0.000000000000000000, 1.000000000000000000 ) ) ;
#11119=LINE ( 'NONE', #470, #3217 ) ;
#11135=AXIS2_PLACEMENT_3D ( 'NONE', #6179, #16166, #19772 ) ;
#11143=CARTESIAN_POINT ( 'NONE',  ( 49.17200000000001836, 6.123233995736769241E-16, -5.000000000000002665 ) ) ;
#11181=VERTEX_POINT ( 'NONE', #2347 ) ;
#11210=AXIS2_PLACEMENT_3D ( 'NONE', #9473, #14914, #3769 ) ;
#11252=CYLINDRICAL_SURFACE ( 'NONE', #13574, 8.000000000000000000 ) ;
#11259=ORIENTED_EDGE ( 'NONE', *, *, #9883, .F. ) ;
#11270=DIRECTION ( 'NONE',  ( 0.000000000000000000, 0.000000000000000000, 1.000000000000000000 ) ) ;
#11312=EDGE_CURVE ( 'NONE', #748, #1893, #10579, .T. ) ;
#11314=CARTESIAN_POINT ( 'NONE',  ( 50.00000000000000000, 0.000000000000000000, 4.171999999999999709 ) ) ;
#11349=DIRECTION ( 'NONE',  ( 0.000000000000000000, 0.4999999999999991118, -0.8660254037844390407 ) ) ;
#11373=FACE_OUTER_BOUND ( 'NONE', #839, .T. ) ;
#11378=DIRECTION ( 'NONE',  ( -1.000000000000000000, -0.000000000000000000, -0.000000000000000000 ) ) ;
#11380=ORIENTED_EDGE ( 'NONE', *, *, #1775, .F. ) ;
#11381=ORIENTED_EDGE ( 'NONE', *, *, #613, .F. ) ;
#11403=ADVANCED_FACE ( 'NONE', ( #3863 ), #3964, .F. ) ;
#11417=EDGE_CURVE ( 'NONE', #10051, #3871, #7969, .T. ) ;
#11420=AXIS2_PLACEMENT_3D ( 'NONE', #7543, #1309, #13028 ) ;
#11474=SHAPE_REPRESENTATION ( 'socket head cap screw_iso_ISO 4762 M10 x 40 - 40N', ( #11210 ), #21934 ) ;
#11485=PRODUCT_DEFINITION_CONTEXT ( 'detailed design', #13123, 'design' ) ;
#11488=DIRECTION ( 'NONE',  ( -1.000000000000000000, -0.000000000000000000, -0.000000000000000000 ) ) ;
#11492=DIRECTION ( 'NONE',  ( 0.000000000000000000, -0.4999999999999987788, 0.8660254037844392627 ) ) ;
#11567=DIRECTION ( 'NONE',  ( 0.000000000000000000, -1.000000000000000000, 0.000000000000000000 ) ) ;
#11573=VECTOR ( 'NONE', #6262, 1000.000000000000000 ) ;
#11603=DIRECTION ( 'NONE',  ( 1.000000000000000000, 0.000000000000000000, 0.000000000000000000 ) ) ;
#11674=ORIENTED_EDGE ( 'NONE', *, *, #20103, .T. ) ;
#11699=DIRECTION ( 'NONE',  ( -1.000000000000000000, -0.000000000000000000, -0.000000000000000000 ) ) ;
#11706=CARTESIAN_POINT ( 'NONE',  ( 5.000000000000000000, 2.342598717236902939, -4.057500000000001883 ) ) ;
#11720=ORIENTED_EDGE ( 'NONE', *, *, #9487, .F. ) ;
#11727=PLANE ( 'NONE',  #23130 ) ;
#11778=ORIENTED_EDGE ( 'NONE', *, *, #6502, .F. ) ;
#11829=EDGE_CURVE ( 'NONE', #5111, #16275, #11119, .T. ) ;
#11849=CIRCLE ( 'NONE', #18339, 0.4000000000000001887 ) ;
#11919=LINE ( 'NONE', #19232, #4866 ) ;
#11953=ORIENTED_EDGE ( 'NONE', *, *, #26, .T. ) ;
#11963=DIRECTION ( 'NONE',  ( 0.000000000000000000, 0.000000000000000000, 1.000000000000000000 ) ) ;
#12015=ORIENTED_EDGE ( 'NONE', *, *, #7182, .F. ) ;
#12057=MANIFOLD_SOLID_BREP ( 'Hex', #15648 ) ;
#12068=ORIENTED_EDGE ( 'NONE', *, *, #23489, .F. ) ;
#12211=CARTESIAN_POINT ( 'NONE',  ( 5.000000000000000000, -4.685197434473811207, 4.770489558936219510E-15 ) ) ;
#12217=DIRECTION ( 'NONE',  ( -1.000000000000000000, -0.000000000000000000, -0.000000000000000000 ) ) ;
#12225=AXIS2_PLACEMENT_3D ( 'NONE', #16901, #15226, #11492 ) ;
#12261=DIRECTION ( 'NONE',  ( 0.000000000000000000, -1.000000000000000000, 9.256405414277014607E-16 ) ) ;
#12287=PLANE ( 'NONE',  #9641 ) ;
#12325=VECTOR ( 'NONE', #10282, 1000.000000000000000 ) ;
#12367=CIRCLE ( 'NONE', #374, 8.000000000000000000 ) ;
#12386=CARTESIAN_POINT ( 'NONE',  ( 10.00000000000000000, 0.000000000000000000, -5.400000000000002132 ) ) ;
#12401=CIRCLE ( 'NONE', #8495, 5.000000000000001776 ) ;
#12453=EDGE_CURVE ( 'NONE', #852, #1893, #3895, .T. ) ;
#12461=PLANE ( 'NONE',  #6519 ) ;
#12542=PRESENTATION_STYLE_ASSIGNMENT (( #16359 ) ) ;
#12610=VERTEX_POINT ( 'NONE', #23200 ) ;
#12693=EDGE_LOOP ( 'NONE', ( #15607, #10110, #16096, #6462 ) ) ;
#12713=DIRECTION ( 'NONE',  ( 0.000000000000000000, 0.000000000000000000, 1.000000000000000000 ) ) ;
#12717=AXIS2_PLACEMENT_3D ( 'NONE', #6367, #18925, #6009 ) ;
#12728=ORIENTED_EDGE ( 'NONE', *, *, #11312, .F. ) ;
#12746=CARTESIAN_POINT ( 'NONE',  ( 10.00000000000000178, 0.000000000000000000, 0.000000000000000000 ) ) ;
#12751=DIRECTION ( 'NONE',  ( 0.000000000000000000, 0.4999999999999989453, -0.8660254037844393737 ) ) ;
#12867=ORIENTED_EDGE ( 'NONE', *, *, #580, .F. ) ;
#12893=VECTOR ( 'NONE', #18378, 999.9999999999998863 ) ;
#12897=CIRCLE ( 'NONE', #9385, 1.499999999999999556 ) ;
#12988=DIRECTION ( 'NONE',  ( 0.000000000000000000, 0.000000000000000000, -1.000000000000000000 ) ) ;
#13000=CARTESIAN_POINT ( 'NONE',  ( 0.000000000000000000, 4.685197434473814759, -5.637851296924623057E-15 ) ) ;
#13028=DIRECTION ( 'NONE',  ( 0.000000000000000000, 0.000000000000000000, 1.000000000000000000 ) ) ;
#13062=ORIENTED_EDGE ( 'NONE', *, *, #747, .T. ) ;
#13084=CARTESIAN_POINT ( 'NONE',  ( -31.74999999999995737, 0.000000000000000000, 0.000000000000000000 ) ) ;
#13123=APPLICATION_CONTEXT ( 'automotive_design' ) ;
#13158=LINE ( 'NONE', #7664, #21792 ) ;
#13186=CARTESIAN_POINT ( 'NONE',  ( 5.000000000000000000, 4.685197434473814759, -5.637851296924623057E-15 ) ) ;
#13270=FACE_OUTER_BOUND ( 'NONE', #12693, .T. ) ;
#13274=DIRECTION ( 'NONE',  ( -1.000000000000000000, -0.000000000000000000, -0.000000000000000000 ) ) ;
#13278=LINE ( 'NONE', #7559, #5698 ) ;
#13336=ORIENTED_EDGE ( 'NONE', *, *, #10514, .F. ) ;
#13360=ADVANCED_FACE ( 'NONE', ( #22123, #4004 ), #16604, .T. ) ;
#13369=DIRECTION ( 'NONE',  ( 0.000000000000000000, 0.000000000000000000, 1.000000000000000000 ) ) ;
#13401=ORIENTED_EDGE ( 'NONE', *, *, #16613, .F. ) ;
#13408=FACE_OUTER_BOUND ( 'NONE', #3527, .T. ) ;
#13431=ORIENTED_EDGE ( 'NONE', *, *, #20489, .T. ) ;
#13471=ORIENTED_EDGE ( 'NONE', *, *, #2973, .F. ) ;
#13488=ORIENTED_EDGE ( 'NONE', *, *, #1025, .T. ) ;
#13535=CARTESIAN_POINT ( 'NONE',  ( -31.74999999999995737, 0.000000000000000000, 0.000000000000000000 ) ) ;
#13548=DIRECTION ( 'NONE',  ( 0.000000000000000000, -0.5000000000000009992, -0.8660254037844380415 ) ) ;
#13565=AXIS2_PLACEMENT_3D ( 'NONE', #20028, #3490, #14853 ) ;
#13570=CARTESIAN_POINT ( 'NONE',  ( 10.00000000000000178, 0.000000000000000000, 8.000000000000000000 ) ) ;
#13574=AXIS2_PLACEMENT_3D ( 'NONE', #3487, #1900, #20026 ) ;
#13592=DIRECTION ( 'NONE',  ( 0.000000000000000000, 0.000000000000000000, -1.000000000000000000 ) ) ;
#13644=CARTESIAN_POINT ( 'NONE',  ( 5.000000000000000000, -2.342598717236900718, 4.057500000000001883 ) ) ;
#13647=SURFACE_STYLE_FILL_AREA ( #23123 ) ;
#13677=EDGE_CURVE ( 'NONE', #3139, #7964, #3154, .T. ) ;
#13704=LINE ( 'NONE', #17512, #16081 ) ;
#13799=TOROIDAL_SURFACE ( 'NONE', #3337, 5.400000000000002132, 0.4000000000000000222 ) ;
#13849=AXIS2_PLACEMENT_3D ( 'NONE', #20485, #2246, #9515 ) ;
#13861=ORIENTED_EDGE ( 'NONE', *, *, #12453, .F. ) ;
#13882=DIRECTION ( 'NONE',  ( 0.000000000000000000, 1.000000000000000000, -1.295896757998781966E-15 ) ) ;
#13890=DIRECTION ( 'NONE',  ( 0.000000000000000000, 0.5000000000000009992, 0.8660254037844380415 ) ) ;
#13974=FACE_OUTER_BOUND ( 'NONE', #3544, .T. ) ;
#13985=EDGE_LOOP ( 'NONE', ( #5778, #2638 ) ) ;
#14003=DIRECTION ( 'NONE',  ( 0.000000000000000000, 0.8660254037844380415, -0.5000000000000009992 ) ) ;
#14100=CARTESIAN_POINT ( 'NONE',  ( 5.000000000000000000, -3.755786496842898268E-15, -4.057500000000000107 ) ) ;
#14114=ORIENTED_EDGE ( 'NONE', *, *, #183, .F. ) ;
#14128=CARTESIAN_POINT ( 'NONE',  ( 5.000000000000000000, 4.685197434473814759, -5.637851296924623057E-15 ) ) ;
#14165=ORIENTED_EDGE ( 'NONE', *, *, #21893, .T. ) ;
#14217=ADVANCED_FACE ( 'NONE', ( #22533 ), #16648, .T. ) ;
#14225=ADVANCED_FACE ( 'NONE', ( #18660 ), #19382, .T. ) ;
#14226=DIRECTION ( 'NONE',  ( 0.000000000000000000, 0.000000000000000000, 1.000000000000000000 ) ) ;
#14343=ORIENTED_EDGE ( 'NONE', *, *, #23070, .T. ) ;
#14408=ORIENTED_EDGE ( 'NONE', *, *, #10982, .T. ) ;
#14418=ORIENTED_EDGE ( 'NONE', *, *, #7127, .T. ) ;
#14469=CARTESIAN_POINT ( 'NONE',  ( 50.00000000000000000, 4.171999999999999709, 0.000000000000000000 ) ) ;
#14478=AXIS2_PLACEMENT_3D ( 'NONE', #1581, #22081, #5555 ) ;
#14480=AXIS2_PLACEMENT_3D ( 'NONE', #18656, #20718, #14956 ) ;
#14613=AXIS2_PLACEMENT_3D ( 'NONE', #1779, #5784, #12713 ) ;
#14771=EDGE_CURVE ( 'NONE', #4158, #6490, #6986, .T. ) ;
#14780=LINE ( 'NONE', #7042, #8464 ) ;
#14804=DIRECTION ( 'NONE',  ( -1.000000000000000000, -0.000000000000000000, -0.000000000000000000 ) ) ;
#14853=DIRECTION ( 'NONE',  ( 0.000000000000000000, 0.000000000000000000, 1.000000000000000000 ) ) ;
#14858=CIRCLE ( 'NONE', #14480, 4.057500000000000107 ) ;
#14893=AXIS2_PLACEMENT_3D ( 'NONE', #10610, #8780, #7180 ) ;
#14914=DIRECTION ( 'NONE',  ( 0.000000000000000000, 0.000000000000000000, 1.000000000000000000 ) ) ;
#14931=ORIENTED_EDGE ( 'NONE', *, *, #747, .F. ) ;
#14956=DIRECTION ( 'NONE',  ( 0.000000000000000000, 0.000000000000000000, 1.000000000000000000 ) ) ;
#14996=CIRCLE ( 'NONE', #21522, 8.000000000000000000 ) ;
#15013=CARTESIAN_POINT ( 'NONE',  ( 10.40000000000000036, 0.000000000000000000, 0.000000000000000000 ) ) ;
#15097=DIRECTION ( 'NONE',  ( 0.000000000000000000, -0.4999999999999991118, 0.8660254037844391517 ) ) ;
#15120=CARTESIAN_POINT ( 'NONE',  ( 0.000000000000000000, 2.342598717236902939, -4.057500000000001883 ) ) ;
#15170=ORIENTED_EDGE ( 'NONE', *, *, #21893, .F. ) ;
#15205=CARTESIAN_POINT ( 'NONE',  ( -31.74999999999995737, 9.797174393178825657E-16, -8.000000000000000000 ) ) ;
#15226=DIRECTION ( 'NONE',  ( -0.000000000000000000, 0.8660254037844393737, 0.4999999999999988343 ) ) ;
#15281=CARTESIAN_POINT ( 'NONE',  ( 5.000000000000000000, 0.000000000000000000, 0.000000000000000000 ) ) ;
#15302=CARTESIAN_POINT ( 'NONE',  ( 0.000000000000000000, -4.685197434473811207, 4.770489558936219510E-15 ) ) ;
#15311=EDGE_LOOP ( 'NONE', ( #105, #3092, #23279, #11381, #17316 ) ) ;
#15319=CARTESIAN_POINT ( 'NONE',  ( 50.00000000000000000, 0.000000000000000000, 0.000000000000000000 ) ) ;
#15333=VERTEX_POINT ( 'NONE', #11314 ) ;
#15337=EDGE_CURVE ( 'NONE', #11181, #1699, #20067, .T. ) ;
#15344=ORIENTED_EDGE ( 'NONE', *, *, #20757, .F. ) ;
#15349=FACE_OUTER_BOUND ( 'NONE', #22595, .T. ) ;
#15361=DIRECTION ( 'NONE',  ( 0.000000000000000000, 1.000000000000000000, -1.224646799147353207E-16 ) ) ;
#15376=AXIS2_PLACEMENT_3D ( 'NONE', #21157, #2793, #1104 ) ;
#15430=DIRECTION ( 'NONE',  ( 0.000000000000000000, -0.4999999999999991118, 0.8660254037844391517 ) ) ;
#15486=DIRECTION ( 'NONE',  ( 0.000000000000000000, -0.5000000000000011102, -0.8660254037844379305 ) ) ;
#15491=CARTESIAN_POINT ( 'NONE',  ( 10.40000000000000036, 6.613092715395709439E-16, 5.400000000000002132 ) ) ;
#15526=ORIENTED_EDGE ( 'NONE', *, *, #10514, .T. ) ;
#15607=ORIENTED_EDGE ( 'NONE', *, *, #23489, .T. ) ;
#15648=CLOSED_SHELL ( 'NONE', ( #10811, #19496, #4296, #7095, #10319, #22271, #19618, #19485, #13360, #4464, #18769, #23307, #16787, #19526, #14217, #7939, #14225, #1338, #8985, #19033, #9959, #3034, #7098, #23338, #11403, #15756, #23571 ) ) ;
#15649=FACE_OUTER_BOUND ( 'NONE', #15311, .T. ) ;
#15682=VERTEX_POINT ( 'NONE', #260 ) ;
#15723=ORIENTED_EDGE ( 'NONE', *, *, #13677, .T. ) ;
#15741=ORIENTED_EDGE ( 'NONE', *, *, #9883, .T. ) ;
#15756=ADVANCED_FACE ( 'NONE', ( #10518 ), #7989, .F. ) ;
#15768=TOROIDAL_SURFACE ( 'NONE', #14613, 6.500000000000000888, 1.500000000000000000 ) ;
#15846=ORIENTED_EDGE ( 'NONE', *, *, #8275, .F. ) ;
#15873=EDGE_CURVE ( 'NONE', #6295, #7126, #18793, .T. ) ;
#15917=( LENGTH_UNIT ( ) NAMED_UNIT ( * ) SI_UNIT ( .MILLI., .METRE. ) );
#15936=DIRECTION ( 'NONE',  ( -0.7071067811865383579, 8.659560562355047490E-17, -0.7071067811865567876 ) ) ;
#16030=PLANE ( 'NONE',  #8827 ) ;
#16039=PLANE ( 'NONE',  #20009 ) ;
#16042=CIRCLE ( 'NONE', #19829, 4.057500000000000107 ) ;
#16061=ORIENTED_EDGE ( 'NONE', *, *, #580, .T. ) ;
#16070=DIRECTION ( 'NONE',  ( -1.000000000000000000, -0.000000000000000000, -0.000000000000000000 ) ) ;
#16081=VECTOR ( 'NONE', #4718, 1000.000000000000000 ) ;
#16096=ORIENTED_EDGE ( 'NONE', *, *, #15873, .T. ) ;
#16130=AXIS2_PLACEMENT_3D ( 'NONE', #18760, #20839, #20578 ) ;
#16154=DIRECTION ( 'NONE',  ( 0.000000000000000000, 0.4999999999999989453, -0.8660254037844393737 ) ) ;
#16166=DIRECTION ( 'NONE',  ( 1.000000000000000000, 0.000000000000000000, 0.000000000000000000 ) ) ;
#16207=CARTESIAN_POINT ( 'NONE',  ( 0.000000000000000000, -4.685197434473811207, 4.770489558936219510E-15 ) ) ;
#16209=VECTOR ( 'NONE', #15486, 1000.000000000000114 ) ;
#16257=( NAMED_UNIT ( * ) SI_UNIT ( $, .STERADIAN. ) SOLID_ANGLE_UNIT ( ) );
#16260=ORIENTED_EDGE ( 'NONE', *, *, #21474, .T. ) ;
#16272=EDGE_CURVE ( 'NONE', #23723, #6529, #18807, .T. ) ;
#16275=VERTEX_POINT ( 'NONE', #23604 ) ;
#16359=SURFACE_STYLE_USAGE ( .BOTH. , #8531 ) ;
#16453=VERTEX_POINT ( 'NONE', #4139 ) ;
#16469=EDGE_LOOP ( 'NONE', ( #15344, #15170, #4897 ) ) ;
#16522=LINE ( 'NONE', #9401, #2599 ) ;
#16535=ORIENTED_EDGE ( 'NONE', *, *, #20348, .F. ) ;
#16550=STYLED_ITEM ( 'NONE', ( #12542 ), #20508 ) ;
#16590=DIRECTION ( 'NONE',  ( 0.000000000000000000, -0.5000000000000011102, -0.8660254037844379305 ) ) ;
#16604=PLANE ( 'NONE',  #17899 ) ;
#16613=EDGE_CURVE ( 'NONE', #15333, #15682, #11919, .T. ) ;
#16648=PLANE ( 'NONE',  #23093 ) ;
#16649=ORIENTED_EDGE ( 'NONE', *, *, #3943, .T. ) ;
#16688=ORIENTED_EDGE ( 'NONE', *, *, #15337, .T. ) ;
#16732=DIRECTION ( 'NONE',  ( -1.000000000000000000, -0.000000000000000000, -0.000000000000000000 ) ) ;
#16733=EDGE_CURVE ( 'NONE', #4339, #15682, #19520, .T. ) ;
#16787=ADVANCED_FACE ( 'NONE', ( #4247 ), #13799, .F. ) ;
#16800=VERTEX_POINT ( 'NONE', #3987 ) ;
#16852=DIRECTION ( 'NONE',  ( -1.000000000000000000, -0.000000000000000000, -0.000000000000000000 ) ) ;
#16898=EDGE_CURVE ( 'NONE', #16800, #4175, #13704, .T. ) ;
#16901=CARTESIAN_POINT ( 'NONE',  ( 5.000000000000000000, -4.685197434473811207, 4.770489558936219510E-15 ) ) ;
#16910=VECTOR ( 'NONE', #15430, 1000.000000000000000 ) ;
#16958=VERTEX_POINT ( 'NONE', #6185 ) ;
#17002=VERTEX_POINT ( 'NONE', #5314 ) ;
#17033=ORIENTED_EDGE ( 'NONE', *, *, #21059, .T. ) ;
#17106=FACE_OUTER_BOUND ( 'NONE', #377, .T. ) ;
#17212=DIRECTION ( 'NONE',  ( 0.000000000000000000, 0.000000000000000000, -1.000000000000000000 ) ) ;
#17232=DIRECTION ( 'NONE',  ( -1.000000000000000000, -0.000000000000000000, -0.000000000000000000 ) ) ;
#17279=LINE ( 'NONE', #12211, #23051 ) ;
#17316=ORIENTED_EDGE ( 'NONE', *, *, #22197, .T. ) ;
#17338=AXIS2_PLACEMENT_3D ( 'NONE', #980, #10445, #4501 ) ;
#17352=LINE ( 'NONE', #21073, #16910 ) ;
#17376=FACE_OUTER_BOUND ( 'NONE', #2429, .T. ) ;
#17427=ORIENTED_EDGE ( 'NONE', *, *, #22741, .F. ) ;
#17435=EDGE_CURVE ( 'NONE', #17002, #4339, #8568, .T. ) ;
#17502=AXIS2_PLACEMENT_3D ( 'NONE', #18943, #2404, #491 ) ;
#17512=CARTESIAN_POINT ( 'NONE',  ( 5.000000000000000000, 4.685197434473814759, -5.637851296924623057E-15 ) ) ;
#17534=EDGE_LOOP ( 'NONE', ( #20865, #16260, #3569, #18809 ) ) ;
#17556=EDGE_LOOP ( 'NONE', ( #4738, #10157 ) ) ;
#17697=CARTESIAN_POINT ( 'NONE',  ( 5.000000000000000000, -2.342598717236900718, 4.057500000000001883 ) ) ;
#17712=FACE_OUTER_BOUND ( 'NONE', #16469, .T. ) ;
#17818=SHAPE_REPRESENTATION_RELATIONSHIP ( 'NONE' , 'NONE' ,  #11474, #20508 ) ;
#17845=AXIS2_PLACEMENT_3D ( 'NONE', #2742, #11603, #8067 ) ;
#17899=AXIS2_PLACEMENT_3D ( 'NONE', #22242, #20551, #20306 ) ;
#18013=CIRCLE ( 'NONE', #1018, 0.4000000000000001887 ) ;
#18090=CIRCLE ( 'NONE', #18467, 5.400000000000002132 ) ;
#18114=VECTOR ( 'NONE', #12751, 999.9999999999998863 ) ;
#18141=CARTESIAN_POINT ( 'NONE',  ( 5.000000000000000000, 2.342598717236902939, -4.057500000000001883 ) ) ;
#18192=DIRECTION ( 'NONE',  ( -1.000000000000000000, -0.000000000000000000, -0.000000000000000000 ) ) ;
#18242=CARTESIAN_POINT ( 'NONE',  ( 5.000000000000000000, -4.685197434473811207, 4.770489558936219510E-15 ) ) ;
#18264=CARTESIAN_POINT ( 'NONE',  ( 5.000000000000000000, 0.000000000000000000, 4.057500000000000107 ) ) ;
#18299=CARTESIAN_POINT ( 'NONE',  ( 10.00000000000000178, 0.000000000000000000, 0.000000000000000000 ) ) ;
#18304=DIRECTION ( 'NONE',  ( 0.000000000000000000, -0.5000000000000009992, -0.8660254037844380415 ) ) ;
#18313=VERTEX_POINT ( 'NONE', #13570 ) ;
#18336=CONICAL_SURFACE ( 'NONE', #14893, 4.171999999999999709, 0.7853981633974613796 ) ;
#18339=AXIS2_PLACEMENT_3D ( 'NONE', #8272, #11567, #17212 ) ;
#18378=DIRECTION ( 'NONE',  ( -0.5000000000000034417, 0.000000000000000000, 0.8660254037844367092 ) ) ;
#18446=TOROIDAL_SURFACE ( 'NONE', #12717, 6.500000000000000888, 1.500000000000000000 ) ;
#18467=AXIS2_PLACEMENT_3D ( 'NONE', #8039, #20701, #20467 ) ;
#18524=ORIENTED_EDGE ( 'NONE', *, *, #4695, .T. ) ;
#18549=CARTESIAN_POINT ( 'NONE',  ( 1.500000000000001332, 0.000000000000000000, 0.000000000000000000 ) ) ;
#18591=ORIENTED_EDGE ( 'NONE', *, *, #6502, .T. ) ;
#18602=ORIENTED_EDGE ( 'NONE', *, *, #4860, .F. ) ;
#18656=CARTESIAN_POINT ( 'NONE',  ( 5.000000000000000000, 0.000000000000000000, 0.000000000000000000 ) ) ;
#18660=FACE_OUTER_BOUND ( 'NONE', #22244, .T. ) ;
#18693=DIRECTION ( 'NONE',  ( 0.000000000000000000, -1.000000000000000000, 9.256405414277014607E-16 ) ) ;
#18721=ORIENTED_EDGE ( 'NONE', *, *, #305, .F. ) ;
#18760=CARTESIAN_POINT ( 'NONE',  ( -31.74999999999995737, 0.000000000000000000, 0.000000000000000000 ) ) ;
#18769=ADVANCED_FACE ( 'NONE', ( #8915 ), #18336, .T. ) ;
#18793=CIRCLE ( 'NONE', #10741, 8.000000000000000000 ) ;
#18807=CIRCLE ( 'NONE', #8423, 6.500000000000000888 ) ;
#18809=ORIENTED_EDGE ( 'NONE', *, *, #16733, .F. ) ;
#18922=LINE ( 'NONE', #15205, #1103 ) ;
#18925=DIRECTION ( 'NONE',  ( -1.000000000000000000, -0.000000000000000000, -0.000000000000000000 ) ) ;
#18943=CARTESIAN_POINT ( 'NONE',  ( 5.000000000000000000, 4.685197434473814759, -5.637851296924623057E-15 ) ) ;
#18979=CARTESIAN_POINT ( 'NONE',  ( 50.00000000000000000, 0.000000000000000000, 0.000000000000000000 ) ) ;
#19003=ORIENTED_EDGE ( 'NONE', *, *, #7871, .T. ) ;
#19033=ADVANCED_FACE ( 'NONE', ( #15649 ), #12287, .F. ) ;
#19047=AXIS2_PLACEMENT_3D ( 'NONE', #7840, #11488, #22439 ) ;
#19062=EDGE_LOOP ( 'NONE', ( #13062, #6792, #14114 ) ) ;
#19129=CYLINDRICAL_SURFACE ( 'NONE', #16130, 8.000000000000000000 ) ;
#19232=CARTESIAN_POINT ( 'NONE',  ( 50.00000000000000000, 0.000000000000000000, 4.171999999999999709 ) ) ;
#19276=CARTESIAN_POINT ( 'NONE',  ( 5.000000000000000000, -2.342598717236900718, 4.057500000000001883 ) ) ;
#19370=DIRECTION ( 'NONE',  ( 0.000000000000000000, -1.000000000000000000, 1.295896757998781966E-15 ) ) ;
#19382=PLANE ( 'NONE',  #1522 ) ;
#19394=LINE ( 'NONE', #20735, #11573 ) ;
#19401=VECTOR ( 'NONE', #10964, 1000.000000000000000 ) ;
#19421=LINE ( 'NONE', #7771, #12325 ) ;
#19477=CARTESIAN_POINT ( 'NONE',  ( 5.000000000000000000, -2.342598717236910488, -4.057499999999997442 ) ) ;
#19485=ADVANCED_FACE ( 'NONE', ( #20253 ), #11252, .T. ) ;
#19496=ADVANCED_FACE ( 'NONE', ( #9406 ), #15768, .T. ) ;
#19507=CARTESIAN_POINT ( 'NONE',  ( 5.000000000000000000, 2.342598717236902939, -4.057500000000001883 ) ) ;
#19515=DIRECTION ( 'NONE',  ( 1.000000000000000000, 0.000000000000000000, 0.000000000000000000 ) ) ;
#19520=CIRCLE ( 'NONE', #22999, 5.000000000000002665 ) ;
#19526=ADVANCED_FACE ( 'NONE', ( #17376 ), #18446, .T. ) ;
#19537=ORIENTED_EDGE ( 'NONE', *, *, #14771, .T. ) ;
#19596=DIRECTION ( 'NONE',  ( 0.000000000000000000, 0.8660254037844380415, -0.5000000000000011102 ) ) ;
#19617=CARTESIAN_POINT ( 'NONE',  ( 5.000000000000000000, -2.342598717236900718, 4.057500000000001883 ) ) ;
#19618=ADVANCED_FACE ( 'NONE', ( #818, #4194 ), #11727, .T. ) ;
#19620=MECHANICAL_DESIGN_GEOMETRIC_PRESENTATION_REPRESENTATION('',(#16550),#10806);
#19712=CARTESIAN_POINT ( 'NONE',  ( 49.17200000000001836, 0.000000000000000000, 0.000000000000000000 ) ) ;
#19766=CARTESIAN_POINT ( 'NONE',  ( 10.00000000000000000, 0.000000000000000000, 0.000000000000000000 ) ) ;
#19772=DIRECTION ( 'NONE',  ( 0.000000000000000000, 0.000000000000000000, -1.000000000000000000 ) ) ;
#19777=ORIENTED_EDGE ( 'NONE', *, *, #11829, .F. ) ;
#19822=( GEOMETRIC_REPRESENTATION_CONTEXT ( 3 ) GLOBAL_UNCERTAINTY_ASSIGNED_CONTEXT ( ( #8082 ) ) GLOBAL_UNIT_ASSIGNED_CONTEXT ( ( #15917, #10864, #6725 ) ) REPRESENTATION_CONTEXT ( 'NONE', 'WORKASPACE' ) );
#19829=AXIS2_PLACEMENT_3D ( 'NONE', #8096, #4935, #1059 ) ;
#19898=EDGE_CURVE ( 'NONE', #6562, #1031, #18090, .T. ) ;
#19925=ORIENTED_EDGE ( 'NONE', *, *, #22741, .T. ) ;
#20009=AXIS2_PLACEMENT_3D ( 'NONE', #14128, #3106, #10508 ) ;
#20026=DIRECTION ( 'NONE',  ( 0.000000000000000000, 0.000000000000000000, 1.000000000000000000 ) ) ;
#20028=CARTESIAN_POINT ( 'NONE',  ( 5.000000000000000000, 0.000000000000000000, 0.000000000000000000 ) ) ;
#20058=DIRECTION ( 'NONE',  ( 0.000000000000000000, 0.000000000000000000, 1.000000000000000000 ) ) ;
#20067=CIRCLE ( 'NONE', #9680, 4.057500000000000107 ) ;
#20103=EDGE_CURVE ( 'NONE', #7964, #11181, #6141, .T. ) ;
#20113=LINE ( 'NONE', #22272, #8809 ) ;
#20150=APPLICATION_CONTEXT ( 'automotive_design' ) ;
#20184=EDGE_LOOP ( 'NONE', ( #8947, #17427, #19537, #13488, #9101, #6654 ) ) ;
#20223=CARTESIAN_POINT ( 'NONE',  ( 1.500000000000001332, 9.797174393178825657E-16, -8.000000000000000000 ) ) ;
#20233=CARTESIAN_POINT ( 'NONE',  ( 0.000000000000000000, -2.342598717236900718, 4.057500000000001883 ) ) ;
#20236=TOROIDAL_SURFACE ( 'NONE', #14478, 5.400000000000002132, 0.4000000000000000222 ) ;
#20253=FACE_OUTER_BOUND ( 'NONE', #239, .T. ) ;
#20306=DIRECTION ( 'NONE',  ( 0.000000000000000000, 0.000000000000000000, -1.000000000000000000 ) ) ;
#20348=EDGE_CURVE ( 'NONE', #7964, #22508, #2559, .T. ) ;
#20378=AXIS2_PLACEMENT_3D ( 'NONE', #13535, #17232, #14226 ) ;
#20392=EDGE_CURVE ( 'NONE', #16958, #9995, #1842, .T. ) ;
#20467=DIRECTION ( 'NONE',  ( 0.000000000000000000, 0.000000000000000000, -1.000000000000000000 ) ) ;
#20485=CARTESIAN_POINT ( 'NONE',  ( 1.500000000000001332, 0.000000000000000000, 6.500000000000000888 ) ) ;
#20489=EDGE_CURVE ( 'NONE', #6750, #18313, #14996, .T. ) ;
#20496=SHAPE_DEFINITION_REPRESENTATION ( #23064, #11474 ) ;
#20508=ADVANCED_BREP_SHAPE_REPRESENTATION ( '', ( #12057, #11210 ), #21934 ) ;
#20551=DIRECTION ( 'NONE',  ( 1.000000000000000000, 0.000000000000000000, 0.000000000000000000 ) ) ;
#20578=DIRECTION ( 'NONE',  ( 0.000000000000000000, 0.000000000000000000, 1.000000000000000000 ) ) ;
#20676=ORIENTED_EDGE ( 'NONE', *, *, #8723, .T. ) ;
#20701=DIRECTION ( 'NONE',  ( -1.000000000000000000, -0.000000000000000000, -0.000000000000000000 ) ) ;
#20718=DIRECTION ( 'NONE',  ( -1.000000000000000000, -0.000000000000000000, -0.000000000000000000 ) ) ;
#20735=CARTESIAN_POINT ( 'NONE',  ( -31.74999999999995737, 0.000000000000000000, 5.000000000000001776 ) ) ;
#20738=ORIENTED_EDGE ( 'NONE', *, *, #20348, .T. ) ;
#20757=EDGE_CURVE ( 'NONE', #12610, #11181, #17279, .T. ) ;
#20837=EDGE_LOOP ( 'NONE', ( #19777, #22882, #17033, #23400, #15741 ) ) ;
#20839=DIRECTION ( 'NONE',  ( -1.000000000000000000, -0.000000000000000000, -0.000000000000000000 ) ) ;
#20850=DIRECTION ( 'NONE',  ( 0.000000000000000000, 1.000000000000000000, -9.256405414277014607E-16 ) ) ;
#20865=ORIENTED_EDGE ( 'NONE', *, *, #17435, .F. ) ;
#20902=CARTESIAN_POINT ( 'NONE',  ( 10.40000000000000036, 6.123233995736768255E-16, -5.000000000000001776 ) ) ;
#20981=ORIENTED_EDGE ( 'NONE', *, *, #11417, .T. ) ;
#21059=EDGE_CURVE ( 'NONE', #10116, #16800, #17352, .T. ) ;
#21073=CARTESIAN_POINT ( 'NONE',  ( 5.000000000000000000, 4.685197434473814759, -5.637851296924623057E-15 ) ) ;
#21115=EDGE_CURVE ( 'NONE', #15682, #4339, #7264, .T. ) ;
#21130=AXIS2_PLACEMENT_3D ( 'NONE', #11706, #9633, #20850 ) ;
#21133=EDGE_LOOP ( 'NONE', ( #966, #5706, #2132 ) ) ;
#21157=CARTESIAN_POINT ( 'NONE',  ( 10.40000000000000036, 0.000000000000000000, 0.000000000000000000 ) ) ;
#21273=ORIENTED_EDGE ( 'NONE', *, *, #20392, .T. ) ;
#21296=DIRECTION ( 'NONE',  ( 0.000000000000000000, 0.000000000000000000, 1.000000000000000000 ) ) ;
#21408=EDGE_CURVE ( 'NONE', #15333, #17002, #3037, .T. ) ;
#21435=CARTESIAN_POINT ( 'NONE',  ( 5.000000000000000000, -4.685197434473811207, 4.770489558936219510E-15 ) ) ;
#21450=DIRECTION ( 'NONE',  ( 0.000000000000000000, 0.000000000000000000, -1.000000000000000000 ) ) ;
#21474=EDGE_CURVE ( 'NONE', #17002, #15333, #9238, .T. ) ;
#21522=AXIS2_PLACEMENT_3D ( 'NONE', #12746, #8846, #20058 ) ;
#21588=EDGE_CURVE ( 'NONE', #11181, #22508, #21754, .T. ) ;
#21601=ORIENTED_EDGE ( 'NONE', *, *, #21115, .T. ) ;
#21604=PLANE ( 'NONE',  #7667 ) ;
#21754=LINE ( 'NONE', #18242, #18114 ) ;
#21776=DIRECTION ( 'NONE',  ( 0.000000000000000000, 0.000000000000000000, 1.000000000000000000 ) ) ;
#21792=VECTOR ( 'NONE', #16732, 1000.000000000000000 ) ;
#21893=EDGE_CURVE ( 'NONE', #1699, #12610, #16522, .T. ) ;
#21907=CARTESIAN_POINT ( 'NONE',  ( 5.000000000000000000, -2.342598717236910488, -4.057499999999997442 ) ) ;
#21933=DIRECTION ( 'NONE',  ( 1.000000000000000000, 0.000000000000000000, 0.000000000000000000 ) ) ;
#21934=( GEOMETRIC_REPRESENTATION_CONTEXT ( 3 ) GLOBAL_UNCERTAINTY_ASSIGNED_CONTEXT ( ( #9183 ) ) GLOBAL_UNIT_ASSIGNED_CONTEXT ( ( #4533, #2481, #8179 ) ) REPRESENTATION_CONTEXT ( 'NONE', 'WORKASPACE' ) );
#21963=VECTOR ( 'NONE', #18304, 1000.000000000000114 ) ;
#22081=DIRECTION ( 'NONE',  ( 1.000000000000000000, 0.000000000000000000, 0.000000000000000000 ) ) ;
#22106=DIRECTION ( 'NONE',  ( 0.000000000000000000, 0.000000000000000000, 1.000000000000000000 ) ) ;
#22123=FACE_BOUND ( 'NONE', #8348, .T. ) ;
#22197=EDGE_CURVE ( 'NONE', #10116, #5111, #20113, .T. ) ;
#22220=LINE ( 'NONE', #7499, #397 ) ;
#22242=CARTESIAN_POINT ( 'NONE',  ( 10.00000000000000000, 8.000000000000000000, 0.000000000000000000 ) ) ;
#22244=EDGE_LOOP ( 'NONE', ( #653, #5093, #14418, #14165, #15526 ) ) ;
#22246=DIRECTION ( 'NONE',  ( 1.000000000000000000, 0.000000000000000000, 0.000000000000000000 ) ) ;
#22271=ADVANCED_FACE ( 'NONE', ( #13270 ), #19129, .T. ) ;
#22272=CARTESIAN_POINT ( 'NONE',  ( 5.000000000000000000, 4.685197434473814759, -5.637851296924623057E-15 ) ) ;
#22282=DIRECTION ( 'NONE',  ( -1.000000000000000000, -0.000000000000000000, -0.000000000000000000 ) ) ;
#22324=ORIENTED_EDGE ( 'NONE', *, *, #11312, .T. ) ;
#22363=EDGE_LOOP ( 'NONE', ( #12068, #1793 ) ) ;
#22401=CARTESIAN_POINT ( 'NONE',  ( -31.74999999999995737, 6.123233995736768255E-16, -5.000000000000001776 ) ) ;
#22439=DIRECTION ( 'NONE',  ( 0.000000000000000000, 0.000000000000000000, 1.000000000000000000 ) ) ;
#22446=AXIS2_PLACEMENT_3D ( 'NONE', #15319, #4545, #11963 ) ;
#22459=ORIENTED_EDGE ( 'NONE', *, *, #21115, .F. ) ;
#22463=ORIENTED_EDGE ( 'NONE', *, *, #13677, .F. ) ;
#22492=CARTESIAN_POINT ( 'NONE',  ( 10.40000000000000036, 0.000000000000000000, 0.000000000000000000 ) ) ;
#22508=VERTEX_POINT ( 'NONE', #19477 ) ;
#22519=PLANE ( 'NONE',  #21130 ) ;
#22533=FACE_OUTER_BOUND ( 'NONE', #20837, .T. ) ;
#22595=EDGE_LOOP ( 'NONE', ( #11778, #1005, #14343, #21273 ) ) ;
#22612=DIRECTION ( 'NONE',  ( 0.000000000000000000, 0.000000000000000000, -1.000000000000000000 ) ) ;
#22613=DIRECTION ( 'NONE',  ( -1.000000000000000000, -0.000000000000000000, -0.000000000000000000 ) ) ;
#22653=LINE ( 'NONE', #7938, #3157 ) ;
#22685=CYLINDRICAL_SURFACE ( 'NONE', #4835, 5.000000000000001776 ) ;
#22705=DIRECTION ( 'NONE',  ( 1.000000000000000000, 0.000000000000000000, 0.000000000000000000 ) ) ;
#22741=EDGE_CURVE ( 'NONE', #4158, #16275, #19421, .T. ) ;
#22772=CARTESIAN_POINT ( 'NONE',  ( 5.000000000000000000, 0.000000000000000000, 0.000000000000000000 ) ) ;
#22808=ORIENTED_EDGE ( 'NONE', *, *, #19898, .T. ) ;
#22809=PLANE ( 'NONE',  #12225 ) ;
#22866=EDGE_LOOP ( 'NONE', ( #7631, #19003, #12015, #11380 ) ) ;
#22882=ORIENTED_EDGE ( 'NONE', *, *, #22197, .F. ) ;
#22996=EDGE_LOOP ( 'NONE', ( #19925, #11259, #14931, #12728, #7479 ) ) ;
#22999=AXIS2_PLACEMENT_3D ( 'NONE', #19712, #1822, #22106 ) ;
#23051=VECTOR ( 'NONE', #16154, 999.9999999999998863 ) ;
#23058=ORIENTED_EDGE ( 'NONE', *, *, #17435, .T. ) ;
#23064=PRODUCT_DEFINITION_SHAPE ( 'NONE', 'NONE',  #5780 ) ;
#23069=CARTESIAN_POINT ( 'NONE',  ( 0.000000000000000000, -2.342598717236900718, 4.057500000000001883 ) ) ;
#23070=EDGE_CURVE ( 'NONE', #15682, #16958, #19394, .T. ) ;
#23093=AXIS2_PLACEMENT_3D ( 'NONE', #13186, #3939, #11349 ) ;
#23123=FILL_AREA_STYLE ('',( #8395 ) ) ;
#23130=AXIS2_PLACEMENT_3D ( 'NONE', #4063, #9770, #583 ) ;
#23200=CARTESIAN_POINT ( 'NONE',  ( 5.000000000000000000, -4.685197434473811207, 4.770489558936219510E-15 ) ) ;
#23234=FACE_OUTER_BOUND ( 'NONE', #22996, .T. ) ;
#23279=ORIENTED_EDGE ( 'NONE', *, *, #3943, .F. ) ;
#23307=ADVANCED_FACE ( 'NONE', ( #4799 ), #12461, .T. ) ;
#23338=ADVANCED_FACE ( 'NONE', ( #10378 ), #16039, .F. ) ;
#23400=ORIENTED_EDGE ( 'NONE', *, *, #16898, .T. ) ;
#23416=DIRECTION ( 'NONE',  ( 0.000000000000000000, 0.000000000000000000, 1.000000000000000000 ) ) ;
#23489=EDGE_CURVE ( 'NONE', #18313, #6750, #12367, .T. ) ;
#23571=ADVANCED_FACE ( 'NONE', ( #4300 ), #6918, .F. ) ;
#23586=CARTESIAN_POINT ( 'NONE',  ( 0.000000000000000000, -2.342598717236910488, -4.057499999999997442 ) ) ;
#23604=CARTESIAN_POINT ( 'NONE',  ( 0.000000000000000000, 2.342598717236912709, 4.057499999999995666 ) ) ;
#23627=AXIS2_PLACEMENT_3D ( 'NONE', #10283, #16070, #23416 ) ;
#23700=DIRECTION ( 'NONE',  ( -1.000000000000000000, -0.000000000000000000, -0.000000000000000000 ) ) ;
#23723=VERTEX_POINT ( 'NONE', #3073 ) ;
#23921=COLOUR_RGB('Black',0.12,0.14,0.17);
#23922=FILL_AREA_STYLE_COLOUR('',#23921);
#23923=FILL_AREA_STYLE('',(#23922));
#23924=SURFACE_STYLE_FILL_AREA(#23923);
#23925=SURFACE_SIDE_STYLE('',(#23924));
#23926=SURFACE_STYLE_USAGE(.BOTH.,#23925);
#23927=PRESENTATION_STYLE_ASSIGNMENT((#23926));
ENDSEC;
END-ISO-10303-21;
